ISO-10303-21;
HEADER;
/* Generated by software containing ST-Developer
 * from STEP Tools, Inc. (www.steptools.com) 
 */

FILE_DESCRIPTION(
/* description */ ('PAT-080'),
/* implementation_level */ '2;1');

FILE_NAME(
/* name */ 'Flat Washer - M8.step',
/* time_stamp */ '2026-10-29T20:13:47-07:00',
/* author */ (''),
/* organization */ (''),
/* preprocessor_version */ 'ST-DEVELOPER v20.2',
/* originating_system */ 'Autodesk Translation Framework v15.17.0.0',
/* authorisation */ '');

FILE_SCHEMA (('AUTOMOTIVE_DESIGN { 1 0 10303 214 3 1 1 }'));
ENDSEC;

DATA;
#10=MECHANICAL_DESIGN_GEOMETRIC_PRESENTATION_REPRESENTATION('',(#263),#6878);
#225=SHAPE_REPRESENTATION_RELATIONSHIP('SRR','None',#6981,#244);
#244=ADVANCED_BREP_SHAPE_REPRESENTATION('',(#279),#6876);
#263=STYLED_ITEM('',(#7136),#279);
#279=MANIFOLD_SOLID_BREP('Body1',#3882);
#353=FACE_BOUND('',#1012,.T.);
#354=FACE_BOUND('',#1014,.T.);
#490=PLANE('',#4476);
#491=PLANE('',#4477);
#711=FACE_OUTER_BOUND('',#1009,.T.);
#712=FACE_OUTER_BOUND('',#1010,.T.);
#713=FACE_OUTER_BOUND('',#1011,.T.);
#714=FACE_OUTER_BOUND('',#1013,.T.);
#1009=EDGE_LOOP('',(#3508,#3509,#3510,#3511));
#1010=EDGE_LOOP('',(#3512,#3513,#3514,#3515));
#1011=EDGE_LOOP('',(#3516));
#1012=EDGE_LOOP('',(#3517));
#1013=EDGE_LOOP('',(#3518));
#1014=EDGE_LOOP('',(#3519));
#1332=LINE('',#6710,#1647);
#1333=LINE('',#6716,#1648);
#1647=VECTOR('',#5594,0.42);
#1648=VECTOR('',#5601,0.8);
#1802=CIRCLE('',#4471,0.42);
#1803=CIRCLE('',#4472,0.42);
#1804=CIRCLE('',#4474,0.8);
#1805=CIRCLE('',#4475,0.8);
#2107=VERTEX_POINT('',#6707);
#2108=VERTEX_POINT('',#6709);
#2109=VERTEX_POINT('',#6713);
#2110=VERTEX_POINT('',#6715);
#2577=EDGE_CURVE('',#2107,#2107,#1802,.T.);
#2578=EDGE_CURVE('',#2107,#2108,#1332,.T.);
#2579=EDGE_CURVE('',#2108,#2108,#1803,.T.);
#2580=EDGE_CURVE('',#2109,#2109,#1804,.T.);
#2581=EDGE_CURVE('',#2109,#2110,#1333,.T.);
#2582=EDGE_CURVE('',#2110,#2110,#1805,.T.);
#3508=ORIENTED_EDGE('',*,*,#2577,.F.);
#3509=ORIENTED_EDGE('',*,*,#2578,.T.);
#3510=ORIENTED_EDGE('',*,*,#2579,.T.);
#3511=ORIENTED_EDGE('',*,*,#2578,.F.);
#3512=ORIENTED_EDGE('',*,*,#2580,.F.);
#3513=ORIENTED_EDGE('',*,*,#2581,.T.);
#3514=ORIENTED_EDGE('',*,*,#2582,.T.);
#3515=ORIENTED_EDGE('',*,*,#2581,.F.);
#3516=ORIENTED_EDGE('',*,*,#2580,.T.);
#3517=ORIENTED_EDGE('',*,*,#2577,.T.);
#3518=ORIENTED_EDGE('',*,*,#2582,.F.);
#3519=ORIENTED_EDGE('',*,*,#2579,.F.);
#3633=CYLINDRICAL_SURFACE('',#4470,0.42);
#3634=CYLINDRICAL_SURFACE('',#4473,0.8);
#3847=ADVANCED_FACE('',(#711),#3633,.F.);
#3848=ADVANCED_FACE('',(#712),#3634,.T.);
#3849=ADVANCED_FACE('',(#713,#353),#490,.T.);
#3850=ADVANCED_FACE('',(#714,#354),#491,.F.);
#3882=CLOSED_SHELL('',(#3847,#3848,#3849,#3850));
#4469=AXIS2_PLACEMENT_3D('',#6705,#5588,#5589);
#4470=AXIS2_PLACEMENT_3D('',#6706,#5590,#5591);
#4471=AXIS2_PLACEMENT_3D('',#6708,#5592,#5593);
#4472=AXIS2_PLACEMENT_3D('',#6711,#5595,#5596);
#4473=AXIS2_PLACEMENT_3D('',#6712,#5597,#5598);
#4474=AXIS2_PLACEMENT_3D('',#6714,#5599,#5600);
#4475=AXIS2_PLACEMENT_3D('',#6717,#5602,#5603);
#4476=AXIS2_PLACEMENT_3D('',#6718,#5604,#5605);
#4477=AXIS2_PLACEMENT_3D('',#6719,#5606,#5607);
#5588=DIRECTION('axis',(0.,0.,1.));
#5589=DIRECTION('refdir',(1.,0.,0.));
#5590=DIRECTION('center_axis',(0.,1.,0.));
#5591=DIRECTION('ref_axis',(1.,0.,0.));
#5592=DIRECTION('center_axis',(0.,-1.,0.));
#5593=DIRECTION('ref_axis',(1.,0.,0.));
#5594=DIRECTION('',(0.,-1.,0.));
#5595=DIRECTION('center_axis',(0.,-1.,0.));
#5596=DIRECTION('ref_axis',(1.,0.,0.));
#5597=DIRECTION('center_axis',(0.,1.,0.));
#5598=DIRECTION('ref_axis',(1.,0.,0.));
#5599=DIRECTION('center_axis',(0.,1.,0.));
#5600=DIRECTION('ref_axis',(1.,0.,0.));
#5601=DIRECTION('',(0.,-1.,0.));
#5602=DIRECTION('center_axis',(0.,1.,0.));
#5603=DIRECTION('ref_axis',(1.,0.,0.));
#5604=DIRECTION('center_axis',(0.,1.,0.));
#5605=DIRECTION('ref_axis',(1.,0.,0.));
#5606=DIRECTION('center_axis',(0.,1.,0.));
#5607=DIRECTION('ref_axis',(1.,0.,0.));
#6705=CARTESIAN_POINT('',(0.,0.,0.));
#6706=CARTESIAN_POINT('Origin',(0.,0.,0.));
#6707=CARTESIAN_POINT('',(-0.42,0.16,5.14351655641888E-17));
#6708=CARTESIAN_POINT('Origin',(0.,0.16,0.));
#6709=CARTESIAN_POINT('',(-0.42,0.,5.14351655641888E-17));
#6710=CARTESIAN_POINT('',(-0.42,0.,5.14351655641888E-17));
#6711=CARTESIAN_POINT('Origin',(0.,0.,0.));
#6712=CARTESIAN_POINT('Origin',(0.,0.,0.));
#6713=CARTESIAN_POINT('',(-0.8,0.16,9.79717439317883E-17));
#6714=CARTESIAN_POINT('Origin',(0.,0.16,0.));
#6715=CARTESIAN_POINT('',(-0.8,0.,9.79717439317883E-17));
#6716=CARTESIAN_POINT('',(-0.8,0.,9.79717439317883E-17));
#6717=CARTESIAN_POINT('Origin',(0.,0.,0.));
#6718=CARTESIAN_POINT('Origin',(0.,0.16,0.));
#6719=CARTESIAN_POINT('Origin',(0.,0.,0.));
#6855=UNCERTAINTY_MEASURE_WITH_UNIT(LENGTH_MEASURE(0.001),#6879,
'DISTANCE_ACCURACY_VALUE',
'Maximum model space distance between geometric entities at asserted c
onnectivities');
#6857=UNCERTAINTY_MEASURE_WITH_UNIT(LENGTH_MEASURE(0.001),#6879,
'DISTANCE_ACCURACY_VALUE',
'Maximum model space distance between geometric entities at asserted c
onnectivities');
#6876=(
GEOMETRIC_REPRESENTATION_CONTEXT(3)
GLOBAL_UNCERTAINTY_ASSIGNED_CONTEXT((#6855))
GLOBAL_UNIT_ASSIGNED_CONTEXT((#6879,#6881,#6882))
REPRESENTATION_CONTEXT('','3D')
);
#6878=(
GEOMETRIC_REPRESENTATION_CONTEXT(3)
GLOBAL_UNCERTAINTY_ASSIGNED_CONTEXT((#6857))
GLOBAL_UNIT_ASSIGNED_CONTEXT((#6879,#6881,#6882))
REPRESENTATION_CONTEXT('','3D')
);
#6879=(
LENGTH_UNIT()
NAMED_UNIT(*)
SI_UNIT(.CENTI.,.METRE.)
);
#6881=(
NAMED_UNIT(*)
PLANE_ANGLE_UNIT()
SI_UNIT($,.RADIAN.)
);
#6882=(
NAMED_UNIT(*)
SI_UNIT($,.STERADIAN.)
SOLID_ANGLE_UNIT()
);
#6901=SHAPE_DEFINITION_REPRESENTATION(#6921,#6981);
#6921=PRODUCT_DEFINITION_SHAPE('',$,#7002);
#6981=SHAPE_REPRESENTATION('',(#4469),#6876);
#6983=PRODUCT_DEFINITION_CONTEXT('part definition',#7045,'design');
#7002=PRODUCT_DEFINITION('Flat Washer - M8','Flat Washer - M8',
#7022,#6983);
#7022=PRODUCT_DEFINITION_FORMATION('',$,#7065);
#7045=APPLICATION_CONTEXT(
'Core Data for Automotive Mechanical Design Process');
#7046=PRODUCT_CONTEXT('part definition',#7045,'mechanical');
#7065=PRODUCT('Flat Washer - M8','Flat Washer - M8',
'Flat Washer - M8',(#7046));
#7130=COLOUR_RGB('Black',0.12,0.14,0.17);
#7131=FILL_AREA_STYLE_COLOUR('',#7130);
#7132=FILL_AREA_STYLE('',(#7131));
#7133=SURFACE_STYLE_FILL_AREA(#7132);
#7134=SURFACE_SIDE_STYLE('',(#7133));
#7135=SURFACE_STYLE_USAGE(.BOTH.,#7134);
#7136=PRESENTATION_STYLE_ASSIGNMENT((#7135));
ENDSEC;
END-ISO-10303-21;
